ISO-10303-21;
HEADER;
/* Generated by software containing ST-Developer
 * from STEP Tools, Inc. (www.steptools.com) 
 */

FILE_DESCRIPTION(
/* description */ ('Ball-race swivel caster'),
/* implementation_level */ '2;1');

FILE_NAME(
/* name */ 'Cage (1).step',
/* time_stamp */ '2026-10-29T16:15:51-07:00',
/* author */ (''),
/* organization */ (''),
/* preprocessor_version */ 'ST-DEVELOPER v20.2',
/* originating_system */ 'Autodesk Translation Framework v15.17.0.0',
/* authorisation */ '');

FILE_SCHEMA (('AUTOMOTIVE_DESIGN { 1 0 10303 214 3 1 1 }'));
ENDSEC;

DATA;
#10=MECHANICAL_DESIGN_GEOMETRIC_PRESENTATION_REPRESENTATION('',(#330),#7816);
#163=SPHERICAL_SURFACE('',#4401,0.309556);
#164=SPHERICAL_SURFACE('',#4417,0.309556);
#165=SPHERICAL_SURFACE('',#4422,0.309556);
#166=SPHERICAL_SURFACE('',#4428,0.309556);
#167=SPHERICAL_SURFACE('',#4433,0.309556);
#168=SPHERICAL_SURFACE('',#4438,0.309556);
#169=SPHERICAL_SURFACE('',#4446,0.309556);
#244=B_SPLINE_CURVE_WITH_KNOTS('',3,(#7318,#7319,#7320,#7321,#7322,#7323,
#7324,#7325,#7326,#7327,#7328,#7329,#7330,#7331,#7332,#7333,#7334,#7335,
#7336,#7337,#7338,#7339),.UNSPECIFIED.,.F.,.F.,(4,2,2,2,2,2,2,2,2,2,4),
(0.0591825211272536,0.157966726598481,0.236950089897721,0.315933453196962,
0.391576304923761,0.46721915665056,0.54286200837736,0.618504860104159,0.697488223403399,
0.77647158670264,0.875255792173867),.UNSPECIFIED.);
#245=B_SPLINE_CURVE_WITH_KNOTS('',3,(#7343,#7344,#7345,#7346,#7347,#7348,
#7349,#7350,#7351,#7352,#7353,#7354,#7355,#7356,#7357,#7358,#7359,#7360,
#7361,#7362,#7363,#7364),.UNSPECIFIED.,.F.,.F.,(4,2,2,2,2,2,2,2,2,2,4),
(0.0581119756758434,0.106553146291161,0.213106292582322,0.30849933801665,
0.386091982889075,0.4636846277615,0.541277272633925,0.61886991750635,0.714262962940678,
0.820816109231839,0.869257279847157),.UNSPECIFIED.);
#246=B_SPLINE_CURVE_WITH_KNOTS('',3,(#7370,#7371,#7372,#7373,#7374,#7375,
#7376,#7377,#7378,#7379,#7380,#7381,#7382,#7383,#7384,#7385,#7386,#7387,
#7388,#7389,#7390,#7391),.UNSPECIFIED.,.F.,.F.,(4,2,2,2,2,2,2,2,2,2,4),
(0.0581119756758434,0.106553146291161,0.213106292582322,0.30849933801665,
0.386091982889075,0.4636846277615,0.541277272633925,0.61886991750635,0.714262962940679,
0.820816109231839,0.869257279847157),.UNSPECIFIED.);
#247=B_SPLINE_CURVE_WITH_KNOTS('',3,(#7395,#7396,#7397,#7398,#7399,#7400,
#7401,#7402,#7403,#7404,#7405,#7406,#7407,#7408,#7409,#7410,#7411,#7412,
#7413,#7414,#7415,#7416),.UNSPECIFIED.,.F.,.F.,(4,2,2,2,2,2,2,2,2,2,4),
(0.0581119756758433,0.106553146291161,0.213106292582322,0.308499338016649,
0.386091982889075,0.4636846277615,0.541277272633925,0.61886991750635,0.714262962940678,
0.820816109231839,0.869257279847157),.UNSPECIFIED.);
#248=B_SPLINE_CURVE_WITH_KNOTS('',3,(#7425,#7426,#7427,#7428,#7429,#7430,
#7431,#7432,#7433,#7434,#7435,#7436,#7437,#7438,#7439,#7440,#7441,#7442,
#7443,#7444,#7445,#7446),.UNSPECIFIED.,.F.,.F.,(4,2,2,2,2,2,2,2,2,2,4),
(0.0581119756758433,0.106553146291161,0.213106292582322,0.30849933801665,
0.386091982889075,0.4636846277615,0.541277272633925,0.61886991750635,0.714262962940678,
0.820816109231839,0.869257279847157),.UNSPECIFIED.);
#249=B_SPLINE_CURVE_WITH_KNOTS('',3,(#7450,#7451,#7452,#7453,#7454,#7455,
#7456,#7457,#7458,#7459,#7460,#7461,#7462,#7463,#7464,#7465,#7466,#7467,
#7468,#7469,#7470,#7471),.UNSPECIFIED.,.F.,.F.,(4,2,2,2,2,2,2,2,2,2,4),
(0.0581119756758434,0.106553146291161,0.213106292582322,0.30849933801665,
0.386091982889075,0.4636846277615,0.541277272633925,0.61886991750635,0.714262962940678,
0.820816109231839,0.869257279847157),.UNSPECIFIED.);
#250=B_SPLINE_CURVE_WITH_KNOTS('',3,(#7475,#7476,#7477,#7478,#7479,#7480,
#7481,#7482,#7483,#7484,#7485,#7486,#7487,#7488,#7489,#7490,#7491,#7492,
#7493,#7494,#7495,#7496),.UNSPECIFIED.,.F.,.F.,(4,2,2,2,2,2,2,2,2,2,4),
(0.0581119756758434,0.106553146291161,0.213106292582322,0.30849933801665,
0.386091982889075,0.4636846277615,0.541277272633925,0.61886991750635,0.714262962940678,
0.820816109231839,0.869257279847157),.UNSPECIFIED.);
#251=B_SPLINE_CURVE_WITH_KNOTS('',3,(#7500,#7501,#7502,#7503,#7504,#7505,
#7506,#7507,#7508,#7509,#7510,#7511,#7512,#7513,#7514,#7515,#7516,#7517,
#7518,#7519,#7520,#7521),.UNSPECIFIED.,.F.,.F.,(4,2,2,2,2,2,2,2,2,2,4),
(0.0581119756758433,0.106553146291161,0.213106292582322,0.30849933801665,
0.386091982889075,0.4636846277615,0.541277272633925,0.61886991750635,0.714262962940678,
0.820816109231839,0.869257279847157),.UNSPECIFIED.);
#252=B_SPLINE_CURVE_WITH_KNOTS('',3,(#7529,#7530,#7531,#7532,#7533,#7534,
#7535,#7536,#7537,#7538,#7539,#7540,#7541,#7542,#7543,#7544,#7545,#7546,
#7547,#7548,#7549,#7550),.UNSPECIFIED.,.F.,.F.,(4,2,2,2,2,2,2,2,2,2,4),
(0.0591825211272536,0.157966726598481,0.236950089897721,0.315933453196962,
0.391576304923761,0.467219156650561,0.54286200837736,0.618504860104159,
0.697488223403399,0.77647158670264,0.875255792173867),.UNSPECIFIED.);
#253=B_SPLINE_CURVE_WITH_KNOTS('',3,(#7558,#7559,#7560,#7561,#7562,#7563,
#7564,#7565,#7566,#7567,#7568,#7569,#7570,#7571,#7572,#7573,#7574,#7575,
#7576,#7577,#7578,#7579),.UNSPECIFIED.,.F.,.F.,(4,2,2,2,2,2,2,2,2,2,4),
(0.0591825211272536,0.157966726598481,0.236950089897722,0.315933453196962,
0.391576304923761,0.467219156650561,0.54286200837736,0.618504860104159,
0.697488223403399,0.77647158670264,0.875255792173867),.UNSPECIFIED.);
#254=B_SPLINE_CURVE_WITH_KNOTS('',3,(#7589,#7590,#7591,#7592,#7593,#7594,
#7595,#7596,#7597,#7598,#7599,#7600,#7601,#7602,#7603,#7604,#7605,#7606,
#7607,#7608,#7609,#7610),.UNSPECIFIED.,.F.,.F.,(4,2,2,2,2,2,2,2,2,2,4),
(0.0591825211272536,0.157966726598481,0.236950089897721,0.315933453196962,
0.391576304923761,0.46721915665056,0.54286200837736,0.618504860104159,0.697488223403399,
0.77647158670264,0.875255792173867),.UNSPECIFIED.);
#255=B_SPLINE_CURVE_WITH_KNOTS('',3,(#7618,#7619,#7620,#7621,#7622,#7623,
#7624,#7625,#7626,#7627,#7628,#7629,#7630,#7631,#7632,#7633,#7634,#7635,
#7636,#7637,#7638,#7639),.UNSPECIFIED.,.F.,.F.,(4,2,2,2,2,2,2,2,2,2,4),
(0.0591825211272536,0.157966726598481,0.236950089897721,0.315933453196962,
0.391576304923761,0.46721915665056,0.542862008377359,0.618504860104159,
0.697488223403399,0.776471586702639,0.875255792173867),.UNSPECIFIED.);
#256=B_SPLINE_CURVE_WITH_KNOTS('',3,(#7647,#7648,#7649,#7650,#7651,#7652,
#7653,#7654,#7655,#7656,#7657,#7658,#7659,#7660,#7661,#7662,#7663,#7664,
#7665,#7666,#7667,#7668),.UNSPECIFIED.,.F.,.F.,(4,2,2,2,2,2,2,2,2,2,4),
(0.0591825211272536,0.157966726598481,0.236950089897721,0.315933453196962,
0.391576304923761,0.46721915665056,0.54286200837736,0.618504860104159,0.697488223403399,
0.77647158670264,0.875255792173867),.UNSPECIFIED.);
#257=B_SPLINE_CURVE_WITH_KNOTS('',3,(#7677,#7678,#7679,#7680,#7681,#7682,
#7683,#7684,#7685,#7686,#7687,#7688,#7689,#7690,#7691,#7692,#7693,#7694,
#7695,#7696,#7697,#7698),.UNSPECIFIED.,.F.,.F.,(4,2,2,2,2,2,2,2,2,2,4),
(0.0591825211272536,0.157966726598481,0.236950089897721,0.315933453196962,
0.391576304923761,0.46721915665056,0.542862008377359,0.618504860104159,
0.697488223403399,0.776471586702639,0.875255792173867),.UNSPECIFIED.);
#275=SHAPE_REPRESENTATION_RELATIONSHIP('SRR','None',#7924,#295);
#295=ADVANCED_BREP_SHAPE_REPRESENTATION('',(#365),#7813);
#330=STYLED_ITEM('',(#8097),#365);
#365=MANIFOLD_SOLID_BREP('Continuous crown cage',#3737);
#431=FACE_BOUND('',#991,.T.);
#510=PLANE('',#4414);
#511=PLANE('',#4419);
#512=PLANE('',#4424);
#513=PLANE('',#4430);
#514=PLANE('',#4435);
#515=PLANE('',#4444);
#516=PLANE('',#4448);
#517=PLANE('',#4449);
#704=FACE_OUTER_BOUND('',#975,.T.);
#705=FACE_OUTER_BOUND('',#976,.T.);
#706=FACE_OUTER_BOUND('',#977,.T.);
#707=FACE_OUTER_BOUND('',#978,.T.);
#708=FACE_OUTER_BOUND('',#979,.T.);
#709=FACE_OUTER_BOUND('',#980,.T.);
#710=FACE_OUTER_BOUND('',#981,.T.);
#711=FACE_OUTER_BOUND('',#982,.T.);
#712=FACE_OUTER_BOUND('',#983,.T.);
#713=FACE_OUTER_BOUND('',#984,.T.);
#714=FACE_OUTER_BOUND('',#985,.T.);
#715=FACE_OUTER_BOUND('',#986,.T.);
#716=FACE_OUTER_BOUND('',#987,.T.);
#717=FACE_OUTER_BOUND('',#988,.T.);
#718=FACE_OUTER_BOUND('',#989,.T.);
#719=FACE_OUTER_BOUND('',#990,.T.);
#720=FACE_OUTER_BOUND('',#992,.T.);
#975=EDGE_LOOP('',(#3295,#3296,#3297,#3298));
#976=EDGE_LOOP('',(#3299,#3300,#3301,#3302,#3303,#3304,#3305,#3306,#3307,
#3308,#3309,#3310,#3311,#3312,#3313,#3314,#3315,#3316));
#977=EDGE_LOOP('',(#3317,#3318,#3319,#3320));
#978=EDGE_LOOP('',(#3321,#3322,#3323,#3324));
#979=EDGE_LOOP('',(#3325,#3326,#3327,#3328));
#980=EDGE_LOOP('',(#3329,#3330,#3331,#3332));
#981=EDGE_LOOP('',(#3333,#3334,#3335,#3336,#3337,#3338));
#982=EDGE_LOOP('',(#3339,#3340,#3341,#3342));
#983=EDGE_LOOP('',(#3343,#3344,#3345,#3346));
#984=EDGE_LOOP('',(#3347,#3348,#3349,#3350));
#985=EDGE_LOOP('',(#3351,#3352,#3353,#3354));
#986=EDGE_LOOP('',(#3355,#3356,#3357,#3358));
#987=EDGE_LOOP('',(#3359,#3360,#3361,#3362,#3363,#3364,#3365,#3366,#3367,
#3368,#3369,#3370,#3371,#3372,#3373,#3374,#3375,#3376));
#988=EDGE_LOOP('',(#3377,#3378,#3379,#3380));
#989=EDGE_LOOP('',(#3381,#3382,#3383,#3384));
#990=EDGE_LOOP('',(#3385));
#991=EDGE_LOOP('',(#3386));
#992=EDGE_LOOP('',(#3387,#3388,#3389,#3390));
#1158=LINE('',#7420,#1313);
#1159=LINE('',#7673,#1314);
#1313=VECTOR('',#5528,1.123812);
#1314=VECTOR('',#5597,1.076188);
#1541=CIRCLE('',#4402,0.303778037777585);
#1542=CIRCLE('',#4403,0.303778037777585);
#1543=CIRCLE('',#4405,1.123812);
#1544=CIRCLE('',#4406,1.123812);
#1545=CIRCLE('',#4407,1.123812);
#1546=CIRCLE('',#4408,1.123812);
#1547=CIRCLE('',#4409,1.123812);
#1548=CIRCLE('',#4410,1.123812);
#1549=CIRCLE('',#4411,1.123812);
#1550=CIRCLE('',#4412,1.123812);
#1551=CIRCLE('',#4413,1.123812);
#1552=CIRCLE('',#4415,1.076188);
#1553=CIRCLE('',#4416,0.303778037777585);
#1554=CIRCLE('',#4418,0.303778037777585);
#1555=CIRCLE('',#4420,1.076188);
#1556=CIRCLE('',#4421,0.303778037777585);
#1557=CIRCLE('',#4423,0.303778037777585);
#1558=CIRCLE('',#4425,1.076188);
#1559=CIRCLE('',#4426,1.076188);
#1560=CIRCLE('',#4427,0.303778037777585);
#1561=CIRCLE('',#4429,0.303778037777585);
#1562=CIRCLE('',#4431,1.076188);
#1563=CIRCLE('',#4432,0.303778037777585);
#1564=CIRCLE('',#4434,0.303778037777585);
#1565=CIRCLE('',#4436,1.076188);
#1566=CIRCLE('',#4437,0.303778037777585);
#1567=CIRCLE('',#4439,0.303778037777585);
#1568=CIRCLE('',#4441,1.076188);
#1569=CIRCLE('',#4442,1.076188);
#1570=CIRCLE('',#4443,1.076188);
#1571=CIRCLE('',#4445,0.303778037777585);
#1572=CIRCLE('',#4447,0.303778037777585);
#1892=VERTEX_POINT('',#7316);
#1893=VERTEX_POINT('',#7317);
#1894=VERTEX_POINT('',#7340);
#1895=VERTEX_POINT('',#7342);
#1896=VERTEX_POINT('',#7367);
#1897=VERTEX_POINT('',#7369);
#1898=VERTEX_POINT('',#7392);
#1899=VERTEX_POINT('',#7394);
#1900=VERTEX_POINT('',#7417);
#1901=VERTEX_POINT('',#7419);
#1902=VERTEX_POINT('',#7422);
#1903=VERTEX_POINT('',#7424);
#1904=VERTEX_POINT('',#7447);
#1905=VERTEX_POINT('',#7449);
#1906=VERTEX_POINT('',#7472);
#1907=VERTEX_POINT('',#7474);
#1908=VERTEX_POINT('',#7497);
#1909=VERTEX_POINT('',#7499);
#1910=VERTEX_POINT('',#7524);
#1911=VERTEX_POINT('',#7528);
#1912=VERTEX_POINT('',#7553);
#1913=VERTEX_POINT('',#7557);
#1914=VERTEX_POINT('',#7582);
#1915=VERTEX_POINT('',#7584);
#1916=VERTEX_POINT('',#7588);
#1917=VERTEX_POINT('',#7613);
#1918=VERTEX_POINT('',#7617);
#1919=VERTEX_POINT('',#7642);
#1920=VERTEX_POINT('',#7646);
#1921=VERTEX_POINT('',#7671);
#1922=VERTEX_POINT('',#7674);
#1923=VERTEX_POINT('',#7676);
#2367=EDGE_CURVE('',#1892,#1893,#244,.T.);
#2368=EDGE_CURVE('',#1894,#1892,#1541,.T.);
#2369=EDGE_CURVE('',#1895,#1894,#245,.T.);
#2370=EDGE_CURVE('',#1893,#1895,#1542,.T.);
#2371=EDGE_CURVE('',#1896,#1894,#1543,.T.);
#2372=EDGE_CURVE('',#1896,#1897,#246,.T.);
#2373=EDGE_CURVE('',#1898,#1897,#1544,.T.);
#2374=EDGE_CURVE('',#1898,#1899,#247,.T.);
#2375=EDGE_CURVE('',#1900,#1899,#1545,.T.);
#2376=EDGE_CURVE('',#1900,#1901,#1158,.T.);
#2377=EDGE_CURVE('',#1901,#1901,#1546,.T.);
#2378=EDGE_CURVE('',#1902,#1900,#1547,.T.);
#2379=EDGE_CURVE('',#1902,#1903,#248,.T.);
#2380=EDGE_CURVE('',#1904,#1903,#1548,.T.);
#2381=EDGE_CURVE('',#1904,#1905,#249,.T.);
#2382=EDGE_CURVE('',#1906,#1905,#1549,.T.);
#2383=EDGE_CURVE('',#1906,#1907,#250,.T.);
#2384=EDGE_CURVE('',#1908,#1907,#1550,.T.);
#2385=EDGE_CURVE('',#1908,#1909,#251,.T.);
#2386=EDGE_CURVE('',#1895,#1909,#1551,.T.);
#2387=EDGE_CURVE('',#1892,#1910,#1552,.T.);
#2388=EDGE_CURVE('',#1910,#1896,#1553,.T.);
#2389=EDGE_CURVE('',#1911,#1910,#252,.T.);
#2390=EDGE_CURVE('',#1897,#1911,#1554,.T.);
#2391=EDGE_CURVE('',#1911,#1912,#1555,.T.);
#2392=EDGE_CURVE('',#1912,#1898,#1556,.T.);
#2393=EDGE_CURVE('',#1913,#1912,#253,.T.);
#2394=EDGE_CURVE('',#1899,#1913,#1557,.T.);
#2395=EDGE_CURVE('',#1913,#1914,#1558,.T.);
#2396=EDGE_CURVE('',#1914,#1915,#1559,.T.);
#2397=EDGE_CURVE('',#1915,#1902,#1560,.T.);
#2398=EDGE_CURVE('',#1916,#1915,#254,.T.);
#2399=EDGE_CURVE('',#1903,#1916,#1561,.T.);
#2400=EDGE_CURVE('',#1916,#1917,#1562,.T.);
#2401=EDGE_CURVE('',#1917,#1904,#1563,.T.);
#2402=EDGE_CURVE('',#1918,#1917,#255,.T.);
#2403=EDGE_CURVE('',#1905,#1918,#1564,.T.);
#2404=EDGE_CURVE('',#1918,#1919,#1565,.T.);
#2405=EDGE_CURVE('',#1919,#1906,#1566,.T.);
#2406=EDGE_CURVE('',#1920,#1919,#256,.T.);
#2407=EDGE_CURVE('',#1907,#1920,#1567,.T.);
#2408=EDGE_CURVE('',#1921,#1921,#1568,.T.);
#2409=EDGE_CURVE('',#1921,#1914,#1159,.T.);
#2410=EDGE_CURVE('',#1922,#1893,#1569,.T.);
#2411=EDGE_CURVE('',#1922,#1923,#257,.T.);
#2412=EDGE_CURVE('',#1920,#1923,#1570,.T.);
#2413=EDGE_CURVE('',#1909,#1922,#1571,.T.);
#2414=EDGE_CURVE('',#1923,#1908,#1572,.T.);
#3295=ORIENTED_EDGE('',*,*,#2367,.F.);
#3296=ORIENTED_EDGE('',*,*,#2368,.F.);
#3297=ORIENTED_EDGE('',*,*,#2369,.F.);
#3298=ORIENTED_EDGE('',*,*,#2370,.F.);
#3299=ORIENTED_EDGE('',*,*,#2369,.T.);
#3300=ORIENTED_EDGE('',*,*,#2371,.F.);
#3301=ORIENTED_EDGE('',*,*,#2372,.T.);
#3302=ORIENTED_EDGE('',*,*,#2373,.F.);
#3303=ORIENTED_EDGE('',*,*,#2374,.T.);
#3304=ORIENTED_EDGE('',*,*,#2375,.F.);
#3305=ORIENTED_EDGE('',*,*,#2376,.T.);
#3306=ORIENTED_EDGE('',*,*,#2377,.F.);
#3307=ORIENTED_EDGE('',*,*,#2376,.F.);
#3308=ORIENTED_EDGE('',*,*,#2378,.F.);
#3309=ORIENTED_EDGE('',*,*,#2379,.T.);
#3310=ORIENTED_EDGE('',*,*,#2380,.F.);
#3311=ORIENTED_EDGE('',*,*,#2381,.T.);
#3312=ORIENTED_EDGE('',*,*,#2382,.F.);
#3313=ORIENTED_EDGE('',*,*,#2383,.T.);
#3314=ORIENTED_EDGE('',*,*,#2384,.F.);
#3315=ORIENTED_EDGE('',*,*,#2385,.T.);
#3316=ORIENTED_EDGE('',*,*,#2386,.F.);
#3317=ORIENTED_EDGE('',*,*,#2368,.T.);
#3318=ORIENTED_EDGE('',*,*,#2387,.T.);
#3319=ORIENTED_EDGE('',*,*,#2388,.T.);
#3320=ORIENTED_EDGE('',*,*,#2371,.T.);
#3321=ORIENTED_EDGE('',*,*,#2389,.F.);
#3322=ORIENTED_EDGE('',*,*,#2390,.F.);
#3323=ORIENTED_EDGE('',*,*,#2372,.F.);
#3324=ORIENTED_EDGE('',*,*,#2388,.F.);
#3325=ORIENTED_EDGE('',*,*,#2390,.T.);
#3326=ORIENTED_EDGE('',*,*,#2391,.T.);
#3327=ORIENTED_EDGE('',*,*,#2392,.T.);
#3328=ORIENTED_EDGE('',*,*,#2373,.T.);
#3329=ORIENTED_EDGE('',*,*,#2393,.F.);
#3330=ORIENTED_EDGE('',*,*,#2394,.F.);
#3331=ORIENTED_EDGE('',*,*,#2374,.F.);
#3332=ORIENTED_EDGE('',*,*,#2392,.F.);
#3333=ORIENTED_EDGE('',*,*,#2394,.T.);
#3334=ORIENTED_EDGE('',*,*,#2395,.T.);
#3335=ORIENTED_EDGE('',*,*,#2396,.T.);
#3336=ORIENTED_EDGE('',*,*,#2397,.T.);
#3337=ORIENTED_EDGE('',*,*,#2378,.T.);
#3338=ORIENTED_EDGE('',*,*,#2375,.T.);
#3339=ORIENTED_EDGE('',*,*,#2398,.F.);
#3340=ORIENTED_EDGE('',*,*,#2399,.F.);
#3341=ORIENTED_EDGE('',*,*,#2379,.F.);
#3342=ORIENTED_EDGE('',*,*,#2397,.F.);
#3343=ORIENTED_EDGE('',*,*,#2399,.T.);
#3344=ORIENTED_EDGE('',*,*,#2400,.T.);
#3345=ORIENTED_EDGE('',*,*,#2401,.T.);
#3346=ORIENTED_EDGE('',*,*,#2380,.T.);
#3347=ORIENTED_EDGE('',*,*,#2402,.F.);
#3348=ORIENTED_EDGE('',*,*,#2403,.F.);
#3349=ORIENTED_EDGE('',*,*,#2381,.F.);
#3350=ORIENTED_EDGE('',*,*,#2401,.F.);
#3351=ORIENTED_EDGE('',*,*,#2403,.T.);
#3352=ORIENTED_EDGE('',*,*,#2404,.T.);
#3353=ORIENTED_EDGE('',*,*,#2405,.T.);
#3354=ORIENTED_EDGE('',*,*,#2382,.T.);
#3355=ORIENTED_EDGE('',*,*,#2383,.F.);
#3356=ORIENTED_EDGE('',*,*,#2405,.F.);
#3357=ORIENTED_EDGE('',*,*,#2406,.F.);
#3358=ORIENTED_EDGE('',*,*,#2407,.F.);
#3359=ORIENTED_EDGE('',*,*,#2408,.F.);
#3360=ORIENTED_EDGE('',*,*,#2409,.T.);
#3361=ORIENTED_EDGE('',*,*,#2395,.F.);
#3362=ORIENTED_EDGE('',*,*,#2393,.T.);
#3363=ORIENTED_EDGE('',*,*,#2391,.F.);
#3364=ORIENTED_EDGE('',*,*,#2389,.T.);
#3365=ORIENTED_EDGE('',*,*,#2387,.F.);
#3366=ORIENTED_EDGE('',*,*,#2367,.T.);
#3367=ORIENTED_EDGE('',*,*,#2410,.F.);
#3368=ORIENTED_EDGE('',*,*,#2411,.T.);
#3369=ORIENTED_EDGE('',*,*,#2412,.F.);
#3370=ORIENTED_EDGE('',*,*,#2406,.T.);
#3371=ORIENTED_EDGE('',*,*,#2404,.F.);
#3372=ORIENTED_EDGE('',*,*,#2402,.T.);
#3373=ORIENTED_EDGE('',*,*,#2400,.F.);
#3374=ORIENTED_EDGE('',*,*,#2398,.T.);
#3375=ORIENTED_EDGE('',*,*,#2396,.F.);
#3376=ORIENTED_EDGE('',*,*,#2409,.F.);
#3377=ORIENTED_EDGE('',*,*,#2370,.T.);
#3378=ORIENTED_EDGE('',*,*,#2386,.T.);
#3379=ORIENTED_EDGE('',*,*,#2413,.T.);
#3380=ORIENTED_EDGE('',*,*,#2410,.T.);
#3381=ORIENTED_EDGE('',*,*,#2385,.F.);
#3382=ORIENTED_EDGE('',*,*,#2414,.F.);
#3383=ORIENTED_EDGE('',*,*,#2411,.F.);
#3384=ORIENTED_EDGE('',*,*,#2413,.F.);
#3385=ORIENTED_EDGE('',*,*,#2377,.T.);
#3386=ORIENTED_EDGE('',*,*,#2408,.T.);
#3387=ORIENTED_EDGE('',*,*,#2407,.T.);
#3388=ORIENTED_EDGE('',*,*,#2412,.T.);
#3389=ORIENTED_EDGE('',*,*,#2414,.T.);
#3390=ORIENTED_EDGE('',*,*,#2384,.T.);
#3487=CYLINDRICAL_SURFACE('',#4404,1.123812);
#3488=CYLINDRICAL_SURFACE('',#4440,1.076188);
#3675=ADVANCED_FACE('',(#704),#163,.F.);
#3676=ADVANCED_FACE('',(#705),#3487,.T.);
#3677=ADVANCED_FACE('',(#706),#510,.T.);
#3678=ADVANCED_FACE('',(#707),#164,.F.);
#3679=ADVANCED_FACE('',(#708),#511,.T.);
#3680=ADVANCED_FACE('',(#709),#165,.F.);
#3681=ADVANCED_FACE('',(#710),#512,.T.);
#3682=ADVANCED_FACE('',(#711),#166,.F.);
#3683=ADVANCED_FACE('',(#712),#513,.T.);
#3684=ADVANCED_FACE('',(#713),#167,.F.);
#3685=ADVANCED_FACE('',(#714),#514,.T.);
#3686=ADVANCED_FACE('',(#715),#168,.F.);
#3687=ADVANCED_FACE('',(#716),#3488,.F.);
#3688=ADVANCED_FACE('',(#717),#515,.T.);
#3689=ADVANCED_FACE('',(#718),#169,.F.);
#3690=ADVANCED_FACE('',(#719,#431),#516,.T.);
#3691=ADVANCED_FACE('',(#720),#517,.T.);
#3737=CLOSED_SHELL('',(#3675,#3676,#3677,#3678,#3679,#3680,#3681,#3682,
#3683,#3684,#3685,#3686,#3687,#3688,#3689,#3690,#3691));
#4400=AXIS2_PLACEMENT_3D('',#7314,#5512,#5513);
#4401=AXIS2_PLACEMENT_3D('',#7315,#5514,#5515);
#4402=AXIS2_PLACEMENT_3D('',#7341,#5516,#5517);
#4403=AXIS2_PLACEMENT_3D('',#7365,#5518,#5519);
#4404=AXIS2_PLACEMENT_3D('',#7366,#5520,#5521);
#4405=AXIS2_PLACEMENT_3D('',#7368,#5522,#5523);
#4406=AXIS2_PLACEMENT_3D('',#7393,#5524,#5525);
#4407=AXIS2_PLACEMENT_3D('',#7418,#5526,#5527);
#4408=AXIS2_PLACEMENT_3D('',#7421,#5529,#5530);
#4409=AXIS2_PLACEMENT_3D('',#7423,#5531,#5532);
#4410=AXIS2_PLACEMENT_3D('',#7448,#5533,#5534);
#4411=AXIS2_PLACEMENT_3D('',#7473,#5535,#5536);
#4412=AXIS2_PLACEMENT_3D('',#7498,#5537,#5538);
#4413=AXIS2_PLACEMENT_3D('',#7522,#5539,#5540);
#4414=AXIS2_PLACEMENT_3D('',#7523,#5541,#5542);
#4415=AXIS2_PLACEMENT_3D('',#7525,#5543,#5544);
#4416=AXIS2_PLACEMENT_3D('',#7526,#5545,#5546);
#4417=AXIS2_PLACEMENT_3D('',#7527,#5547,#5548);
#4418=AXIS2_PLACEMENT_3D('',#7551,#5549,#5550);
#4419=AXIS2_PLACEMENT_3D('',#7552,#5551,#5552);
#4420=AXIS2_PLACEMENT_3D('',#7554,#5553,#5554);
#4421=AXIS2_PLACEMENT_3D('',#7555,#5555,#5556);
#4422=AXIS2_PLACEMENT_3D('',#7556,#5557,#5558);
#4423=AXIS2_PLACEMENT_3D('',#7580,#5559,#5560);
#4424=AXIS2_PLACEMENT_3D('',#7581,#5561,#5562);
#4425=AXIS2_PLACEMENT_3D('',#7583,#5563,#5564);
#4426=AXIS2_PLACEMENT_3D('',#7585,#5565,#5566);
#4427=AXIS2_PLACEMENT_3D('',#7586,#5567,#5568);
#4428=AXIS2_PLACEMENT_3D('',#7587,#5569,#5570);
#4429=AXIS2_PLACEMENT_3D('',#7611,#5571,#5572);
#4430=AXIS2_PLACEMENT_3D('',#7612,#5573,#5574);
#4431=AXIS2_PLACEMENT_3D('',#7614,#5575,#5576);
#4432=AXIS2_PLACEMENT_3D('',#7615,#5577,#5578);
#4433=AXIS2_PLACEMENT_3D('',#7616,#5579,#5580);
#4434=AXIS2_PLACEMENT_3D('',#7640,#5581,#5582);
#4435=AXIS2_PLACEMENT_3D('',#7641,#5583,#5584);
#4436=AXIS2_PLACEMENT_3D('',#7643,#5585,#5586);
#4437=AXIS2_PLACEMENT_3D('',#7644,#5587,#5588);
#4438=AXIS2_PLACEMENT_3D('',#7645,#5589,#5590);
#4439=AXIS2_PLACEMENT_3D('',#7669,#5591,#5592);
#4440=AXIS2_PLACEMENT_3D('',#7670,#5593,#5594);
#4441=AXIS2_PLACEMENT_3D('',#7672,#5595,#5596);
#4442=AXIS2_PLACEMENT_3D('',#7675,#5598,#5599);
#4443=AXIS2_PLACEMENT_3D('',#7699,#5600,#5601);
#4444=AXIS2_PLACEMENT_3D('',#7700,#5602,#5603);
#4445=AXIS2_PLACEMENT_3D('',#7701,#5604,#5605);
#4446=AXIS2_PLACEMENT_3D('',#7702,#5606,#5607);
#4447=AXIS2_PLACEMENT_3D('',#7703,#5608,#5609);
#4448=AXIS2_PLACEMENT_3D('',#7704,#5610,#5611);
#4449=AXIS2_PLACEMENT_3D('',#7705,#5612,#5613);
#5512=DIRECTION('axis',(0.,0.,1.));
#5513=DIRECTION('refdir',(1.,0.,0.));
#5514=DIRECTION('center_axis',(0.,0.,1.));
#5515=DIRECTION('ref_axis',(1.,0.,0.));
#5516=DIRECTION('center_axis',(0.,-1.,0.));
#5517=DIRECTION('ref_axis',(0.,0.,-1.));
#5518=DIRECTION('center_axis',(0.,-1.,0.));
#5519=DIRECTION('ref_axis',(0.,0.,-1.));
#5520=DIRECTION('center_axis',(0.,1.,0.));
#5521=DIRECTION('ref_axis',(1.,0.,0.));
#5522=DIRECTION('center_axis',(0.,1.,0.));
#5523=DIRECTION('ref_axis',(1.,0.,0.));
#5524=DIRECTION('center_axis',(0.,1.,0.));
#5525=DIRECTION('ref_axis',(1.,0.,0.));
#5526=DIRECTION('center_axis',(0.,1.,0.));
#5527=DIRECTION('ref_axis',(1.,0.,0.));
#5528=DIRECTION('',(0.,-1.,0.));
#5529=DIRECTION('center_axis',(0.,-1.,0.));
#5530=DIRECTION('ref_axis',(1.,0.,0.));
#5531=DIRECTION('center_axis',(0.,1.,0.));
#5532=DIRECTION('ref_axis',(1.,0.,0.));
#5533=DIRECTION('center_axis',(0.,1.,0.));
#5534=DIRECTION('ref_axis',(1.,0.,0.));
#5535=DIRECTION('center_axis',(0.,1.,0.));
#5536=DIRECTION('ref_axis',(1.,0.,0.));
#5537=DIRECTION('center_axis',(0.,1.,0.));
#5538=DIRECTION('ref_axis',(1.,0.,0.));
#5539=DIRECTION('center_axis',(0.,1.,0.));
#5540=DIRECTION('ref_axis',(1.,0.,0.));
#5541=DIRECTION('center_axis',(0.,1.,0.));
#5542=DIRECTION('ref_axis',(1.,0.,0.));
#5543=DIRECTION('center_axis',(0.,-1.,0.));
#5544=DIRECTION('ref_axis',(1.,0.,0.));
#5545=DIRECTION('center_axis',(0.,-1.,0.));
#5546=DIRECTION('ref_axis',(0.,0.,-1.));
#5547=DIRECTION('center_axis',(8.96625347776458E-17,0.,1.));
#5548=DIRECTION('ref_axis',(1.,0.,0.));
#5549=DIRECTION('center_axis',(0.,-1.,0.));
#5550=DIRECTION('ref_axis',(0.,0.,-1.));
#5551=DIRECTION('center_axis',(0.,1.,0.));
#5552=DIRECTION('ref_axis',(1.,0.,0.));
#5553=DIRECTION('center_axis',(0.,-1.,0.));
#5554=DIRECTION('ref_axis',(1.,0.,0.));
#5555=DIRECTION('center_axis',(0.,-1.,0.));
#5556=DIRECTION('ref_axis',(0.,0.,-1.));
#5557=DIRECTION('center_axis',(0.,0.,1.));
#5558=DIRECTION('ref_axis',(1.,0.,0.));
#5559=DIRECTION('center_axis',(0.,-1.,0.));
#5560=DIRECTION('ref_axis',(0.,0.,-1.));
#5561=DIRECTION('center_axis',(0.,1.,0.));
#5562=DIRECTION('ref_axis',(1.,0.,0.));
#5563=DIRECTION('center_axis',(0.,-1.,0.));
#5564=DIRECTION('ref_axis',(1.,0.,0.));
#5565=DIRECTION('center_axis',(0.,-1.,0.));
#5566=DIRECTION('ref_axis',(1.,0.,0.));
#5567=DIRECTION('center_axis',(0.,-1.,0.));
#5568=DIRECTION('ref_axis',(0.,0.,-1.));
#5569=DIRECTION('center_axis',(0.,0.,1.));
#5570=DIRECTION('ref_axis',(1.,0.,0.));
#5571=DIRECTION('center_axis',(0.,-1.,0.));
#5572=DIRECTION('ref_axis',(0.,0.,-1.));
#5573=DIRECTION('center_axis',(0.,1.,0.));
#5574=DIRECTION('ref_axis',(1.,0.,0.));
#5575=DIRECTION('center_axis',(0.,-1.,0.));
#5576=DIRECTION('ref_axis',(1.,0.,0.));
#5577=DIRECTION('center_axis',(0.,-1.,0.));
#5578=DIRECTION('ref_axis',(0.,0.,-1.));
#5579=DIRECTION('center_axis',(8.96625347776458E-17,0.,1.));
#5580=DIRECTION('ref_axis',(1.,0.,0.));
#5581=DIRECTION('center_axis',(0.,-1.,0.));
#5582=DIRECTION('ref_axis',(0.,0.,-1.));
#5583=DIRECTION('center_axis',(0.,1.,0.));
#5584=DIRECTION('ref_axis',(1.,0.,0.));
#5585=DIRECTION('center_axis',(0.,-1.,0.));
#5586=DIRECTION('ref_axis',(1.,0.,0.));
#5587=DIRECTION('center_axis',(0.,-1.,0.));
#5588=DIRECTION('ref_axis',(0.,0.,-1.));
#5589=DIRECTION('center_axis',(0.,0.,1.));
#5590=DIRECTION('ref_axis',(1.,0.,0.));
#5591=DIRECTION('center_axis',(0.,-1.,0.));
#5592=DIRECTION('ref_axis',(0.,0.,-1.));
#5593=DIRECTION('center_axis',(0.,1.,0.));
#5594=DIRECTION('ref_axis',(1.,0.,0.));
#5595=DIRECTION('center_axis',(0.,1.,0.));
#5596=DIRECTION('ref_axis',(1.,0.,0.));
#5597=DIRECTION('',(0.,1.,0.));
#5598=DIRECTION('center_axis',(0.,-1.,0.));
#5599=DIRECTION('ref_axis',(1.,0.,0.));
#5600=DIRECTION('center_axis',(0.,-1.,0.));
#5601=DIRECTION('ref_axis',(1.,0.,0.));
#5602=DIRECTION('center_axis',(0.,1.,0.));
#5603=DIRECTION('ref_axis',(1.,0.,0.));
#5604=DIRECTION('center_axis',(0.,-1.,0.));
#5605=DIRECTION('ref_axis',(0.,0.,-1.));
#5606=DIRECTION('center_axis',(0.,0.,1.));
#5607=DIRECTION('ref_axis',(1.,0.,0.));
#5608=DIRECTION('center_axis',(0.,-1.,0.));
#5609=DIRECTION('ref_axis',(0.,0.,-1.));
#5610=DIRECTION('center_axis',(0.,-1.,0.));
#5611=DIRECTION('ref_axis',(-1.,0.,0.));
#5612=DIRECTION('center_axis',(0.,1.,0.));
#5613=DIRECTION('ref_axis',(1.,0.,0.));
#7314=CARTESIAN_POINT('',(0.,0.,0.));
#7315=CARTESIAN_POINT('Origin',(0.685838782044607,0.,0.860014630714833));
#7316=CARTESIAN_POINT('',(0.413083465285518,-0.05953,0.993751811093549));
#7317=CARTESIAN_POINT('',(0.876916659919095,-0.05953,0.623857181492959));
#7318=CARTESIAN_POINT('Ctrl Pts',(0.413083465285518,-0.05953,0.993751811093549));
#7319=CARTESIAN_POINT('Ctrl Pts',(0.419070565453383,-0.0925528133349865,
0.991263089003441));
#7320=CARTESIAN_POINT('Ctrl Pts',(0.430199341854858,-0.124911173756694,
0.986608710139579));
#7321=CARTESIAN_POINT('Ctrl Pts',(0.457978755888596,-0.177924977804098,
0.973971221090534));
#7322=CARTESIAN_POINT('Ctrl Pts',(0.473077587363685,-0.199697230012983,
0.966820759530997));
#7323=CARTESIAN_POINT('Ctrl Pts',(0.507057380724533,-0.237895043532788,
0.949440676105255));
#7324=CARTESIAN_POINT('Ctrl Pts',(0.525933334162555,-0.254319232363049,
0.939198248544428));
#7325=CARTESIAN_POINT('Ctrl Pts',(0.564362943424238,-0.28018331644634,0.916597376014514));
#7326=CARTESIAN_POINT('Ctrl Pts',(0.585840553788742,-0.29104845371857,0.903141581680914));
#7327=CARTESIAN_POINT('Ctrl Pts',(0.629305439856167,-0.30527573347708,0.873412008702649));
#7328=CARTESIAN_POINT('Ctrl Pts',(0.651278921914856,-0.308638795020976,
0.857118508332695));
#7329=CARTESIAN_POINT('Ctrl Pts',(0.690705563850638,-0.308638795020976,
0.825676810575914));
#7330=CARTESIAN_POINT('Ctrl Pts',(0.711480111898423,-0.30527573347708,0.807879894508811));
#7331=CARTESIAN_POINT('Ctrl Pts',(0.750136149454208,-0.29104845371857,0.772120216227122));
#7332=CARTESIAN_POINT('Ctrl Pts',(0.768033796848072,-0.28018331644634,0.754175290318038));
#7333=CARTESIAN_POINT('Ctrl Pts',(0.798619410861634,-0.254319232363049,
0.721738358858166));
#7334=CARTESIAN_POINT('Ctrl Pts',(0.812805334167529,-0.237895043532788,
0.705614819529209));
#7335=CARTESIAN_POINT('Ctrl Pts',(0.837310877969633,-0.199697230012983,
0.676354402927683));
#7336=CARTESIAN_POINT('Ctrl Pts',(0.847641868610495,-0.177924977804098,
0.663225258065736));
#7337=CARTESIAN_POINT('Ctrl Pts',(0.866144010579847,-0.124911173756694,
0.638954437806245));
#7338=CARTESIAN_POINT('Ctrl Pts',(0.873158080166742,-0.0925528133349865,
0.62914037979579));
#7339=CARTESIAN_POINT('Ctrl Pts',(0.876916659919095,-0.05953,0.623857181492959));
#7340=CARTESIAN_POINT('',(0.437601487681057,-0.05953,1.03511272300331));
#7341=CARTESIAN_POINT('Origin',(0.685838782044607,-0.05953,0.860014630714833));
#7342=CARTESIAN_POINT('',(0.911784794170997,-0.05953,0.656964154625313));
#7343=CARTESIAN_POINT('Ctrl Pts',(0.911784794170998,-0.0595300000000001,
0.656964154625312));
#7344=CARTESIAN_POINT('Ctrl Pts',(0.909827729890942,-0.0762225747374255,
0.659680317203144));
#7345=CARTESIAN_POINT('Ctrl Pts',(0.907004864562642,-0.0928409665394228,
0.663576540841106));
#7346=CARTESIAN_POINT('Ctrl Pts',(0.895234408667242,-0.144299303100741,
0.679480524217551));
#7347=CARTESIAN_POINT('Ctrl Pts',(0.882797231409153,-0.177024326825049,
0.695831250979106));
#7348=CARTESIAN_POINT('Ctrl Pts',(0.854332839576145,-0.227269801620064,
0.73042219438957));
#7349=CARTESIAN_POINT('Ctrl Pts',(0.834863020612702,-0.251265615809407,
0.752807465209441));
#7350=CARTESIAN_POINT('Ctrl Pts',(0.800439809856111,-0.279889827963178,
0.789147407129766));
#7351=CARTESIAN_POINT('Ctrl Pts',(0.781998747691871,-0.290879136862659,
0.80756613568454));
#7352=CARTESIAN_POINT('Ctrl Pts',(0.742239891936898,-0.305251990234487,
0.844254137480382));
#7353=CARTESIAN_POINT('Ctrl Pts',(0.720906778729541,-0.308638795020976,
0.862505527716294));
#7354=CARTESIAN_POINT('Ctrl Pts',(0.680463863683392,-0.308638795020976,
0.894757676234429));
#7355=CARTESIAN_POINT('Ctrl Pts',(0.657923009631182,-0.305251990234488,
0.91149460735272));
#7356=CARTESIAN_POINT('Ctrl Pts',(0.613307674922609,-0.290879136862659,
0.942092777160053));
#7357=CARTESIAN_POINT('Ctrl Pts',(0.591247219971725,-0.279889827963178,
0.955972930713954));
#7358=CARTESIAN_POINT('Ctrl Pts',(0.548158511259202,-0.251265615809407,
0.981446681891443));
#7359=CARTESIAN_POINT('Ctrl Pts',(0.522002043615455,-0.227269801620063,
0.995447160474328));
#7360=CARTESIAN_POINT('Ctrl Pts',(0.481944444320713,-0.177024326825049,
1.01550068154148));
#7361=CARTESIAN_POINT('Ctrl Pts',(0.463236132117164,-0.14429930310074,1.0239876538093));
#7362=CARTESIAN_POINT('Ctrl Pts',(0.445111721969657,-0.0928409665394226,
1.03192403056628));
#7363=CARTESIAN_POINT('Ctrl Pts',(0.440685038163619,-0.0762225747374254,
1.03380912944435));
#7364=CARTESIAN_POINT('Ctrl Pts',(0.437601487681056,-0.05953,1.03511272300331));
#7365=CARTESIAN_POINT('Origin',(0.685838782044607,-0.05953,0.860014630714833));
#7366=CARTESIAN_POINT('Origin',(0.,-0.208355,0.));
#7367=CARTESIAN_POINT('',(0.0548532617164168,-0.05953,1.12247250791415));
#7368=CARTESIAN_POINT('Origin',(0.,-0.05953,0.));
#7369=CARTESIAN_POINT('',(-0.536443649899848,-0.05953,0.987512846410683));
#7370=CARTESIAN_POINT('Ctrl Pts',(0.0548532617164173,-0.0595300000000001,
1.12247250791414));
#7371=CARTESIAN_POINT('Ctrl Pts',(0.05150947068137,-0.0762225747374254,
1.12263591311425));
#7372=CARTESIAN_POINT('Ctrl Pts',(0.0467032526342597,-0.0928409665394227,
1.12285816383385));
#7373=CARTESIAN_POINT('Ctrl Pts',(0.0269302585198975,-0.144299303100741,
1.12357162229597));
#7374=CARTESIAN_POINT('Ctrl Pts',(0.006392292392153,-0.177024326825049,
1.12404235695137));
#7375=CARTESIAN_POINT('Ctrl Pts',(-0.0383992541984087,-0.227269801620063,
1.12335509974011));
#7376=CARTESIAN_POINT('Ctrl Pts',(-0.0680399972366993,-0.251265615809407,
1.12208997038458));
#7377=CARTESIAN_POINT('Ctrl Pts',(-0.117914228755037,-0.279889827963178,
1.1178344036749));
#7378=CARTESIAN_POINT('Ctrl Pts',(-0.14381238480104,-0.290879136862659,
1.11490049012186));
#7379=CARTESIAN_POINT('Ctrl Pts',(-0.19728546073067,-0.305251990234488,
1.10669035995599));
#7380=CARTESIAN_POINT('Ctrl Pts',(-0.224855950742601,-0.308638795020976,
1.10139101611326));
#7381=CARTESIAN_POINT('Ctrl Pts',(-0.275287440920027,-0.308638795020976,
1.0898803575765));
#7382=CARTESIAN_POINT('Ctrl Pts',(-0.302426893214945,-0.305251990234488,
1.08269251410343));
#7383=CARTESIAN_POINT('Ctrl Pts',(-0.35416671187353,-0.290879136862659,
1.06688848765783));
#7384=CARTESIAN_POINT('Ctrl Pts',(-0.3787731215897,-0.279889827963178,1.05829506364875));
#7385=CARTESIAN_POINT('Ctrl Pts',(-0.425554672694338,-0.251265615809407,
1.04048957871266));
#7386=CARTESIAN_POINT('Ctrl Pts',(-0.452808978448581,-0.227269801620063,
1.02876878445619));
#7387=CARTESIAN_POINT('Ctrl Pts',(-0.493462957200432,-0.177024326825049,
1.0099536580922));
#7388=CARTESIAN_POINT('Ctrl Pts',(-0.511762781179148,-0.14429930310074,
1.00061845128527));
#7389=CARTESIAN_POINT('Ctrl Pts',(-0.529268075276157,-0.0928409665394226,
0.991396466802468));
#7390=CARTESIAN_POINT('Ctrl Pts',(-0.533501897135713,-0.0762225747374254,
0.989110885965947));
#7391=CARTESIAN_POINT('Ctrl Pts',(-0.536443649899848,-0.0595300000000001,
0.987512846410683));
#7392=CARTESIAN_POINT('',(-0.843383895613249,-0.05953,0.742736168477219));
#7393=CARTESIAN_POINT('Origin',(0.,-0.05953,0.));
#7394=CARTESIAN_POINT('',(-1.10653577764992,-0.05953,0.196295654879792));
#7395=CARTESIAN_POINT('Ctrl Pts',(-0.843383895613249,-0.0595300000000001,
0.742736168477219));
#7396=CARTESIAN_POINT('Ctrl Pts',(-0.84559647055299,-0.0762225747374255,
0.740223768851062));
#7397=CARTESIAN_POINT('Ctrl Pts',(-0.848766861100456,-0.0928409665394227,
0.736604687327351));
#7398=CARTESIAN_POINT('Ctrl Pts',(-0.861652925570091,-0.144299303100741,
0.721590372101268));
#7399=CARTESIAN_POINT('Ctrl Pts',(-0.87482617317514,-0.177024326825049,
0.705826641853758));
#7400=CARTESIAN_POINT('Ctrl Pts',(-0.902215926359523,-0.227269801620063,
0.670378702718353));
#7401=CARTESIAN_POINT('Ctrl Pts',(-0.919707509403859,-0.251265615809407,
0.646415841396062));
#7402=CARTESIAN_POINT('Ctrl Pts',(-0.947476448101718,-0.279889827963178,
0.604769294586516));
#7403=CARTESIAN_POINT('Ctrl Pts',(-0.961329858300736,-0.290879136862659,
0.582692035672022));
#7404=CARTESIAN_POINT('Ctrl Pts',(-0.988250837578047,-0.305251990234488,
0.535766169015486));
#7405=CARTESIAN_POINT('Ctrl Pts',(-1.00129756308006,-0.308638795020976,
0.510906605094603));
#7406=CARTESIAN_POINT('Ctrl Pts',(-1.02374168767024,-0.308638795020976,
0.46430090015576));
#7407=CARTESIAN_POINT('Ctrl Pts',(-1.03504317708586,-0.305251990234488,
0.438600874831839));
#7408=CARTESIAN_POINT('Ctrl Pts',(-1.05494634094458,-0.290879136862659,
0.388295406390235));
#7409=CARTESIAN_POINT('Ctrl Pts',(-1.06356957703048,-0.279889827963178,
0.363699428370917));
#7410=CARTESIAN_POINT('Ctrl Pts',(-1.0788165083757,-0.251265615809407,0.316022600643821));
#7411=CARTESIAN_POINT('Ctrl Pts',(-1.08664560412098,-0.227269801620063,
0.287406530683752));
#7412=CARTESIAN_POINT('Ctrl Pts',(-1.09728268713976,-0.177024326825049,
0.243890930799337));
#7413=CARTESIAN_POINT('Ctrl Pts',(-1.10139388218929,-0.144299303100741,
0.22376314604679));
#7414=CARTESIAN_POINT('Ctrl Pts',(-1.10509821673782,-0.0928409665394227,
0.204327142733961));
#7415=CARTESIAN_POINT('Ctrl Pts',(-1.10595102243643,-0.0762225747374254,
0.199591971170104));
#7416=CARTESIAN_POINT('Ctrl Pts',(-1.10653577764992,-0.0595300000000001,
0.196295654879792));
#7417=CARTESIAN_POINT('',(-1.123812,-0.05953,1.37627276864339E-16));
#7418=CARTESIAN_POINT('Origin',(0.,-0.05953,0.));
#7419=CARTESIAN_POINT('',(-1.123812,-0.35718,1.37627276864339E-16));
#7420=CARTESIAN_POINT('',(-1.123812,-0.208355,1.37627276864339E-16));
#7421=CARTESIAN_POINT('Origin',(0.,-0.35718,0.));
#7422=CARTESIAN_POINT('',(-1.10653577764992,-0.05953,-0.196295654879793));
#7423=CARTESIAN_POINT('Origin',(0.,-0.05953,0.));
#7424=CARTESIAN_POINT('',(-0.843383895613249,-0.05953,-0.742736168477219));
#7425=CARTESIAN_POINT('Ctrl Pts',(-1.10653577764992,-0.0595300000000001,
-0.196295654879792));
#7426=CARTESIAN_POINT('Ctrl Pts',(-1.10595102243643,-0.0762225747374255,
-0.199591971170104));
#7427=CARTESIAN_POINT('Ctrl Pts',(-1.10509821673782,-0.0928409665394228,
-0.204327142733962));
#7428=CARTESIAN_POINT('Ctrl Pts',(-1.10139388218929,-0.144299303100741,
-0.22376314604679));
#7429=CARTESIAN_POINT('Ctrl Pts',(-1.09728268713976,-0.177024326825049,
-0.243890930799338));
#7430=CARTESIAN_POINT('Ctrl Pts',(-1.08664560412098,-0.227269801620063,
-0.287406530683753));
#7431=CARTESIAN_POINT('Ctrl Pts',(-1.0788165083757,-0.251265615809407,-0.316022600643821));
#7432=CARTESIAN_POINT('Ctrl Pts',(-1.06356957703048,-0.279889827963178,
-0.363699428370918));
#7433=CARTESIAN_POINT('Ctrl Pts',(-1.05494634094458,-0.290879136862659,
-0.388295406390235));
#7434=CARTESIAN_POINT('Ctrl Pts',(-1.03504317708586,-0.305251990234488,
-0.438600874831839));
#7435=CARTESIAN_POINT('Ctrl Pts',(-1.02374168767024,-0.308638795020976,
-0.46430090015576));
#7436=CARTESIAN_POINT('Ctrl Pts',(-1.00129756308006,-0.308638795020976,
-0.510906605094603));
#7437=CARTESIAN_POINT('Ctrl Pts',(-0.988250837578047,-0.305251990234488,
-0.535766169015486));
#7438=CARTESIAN_POINT('Ctrl Pts',(-0.961329858300736,-0.290879136862659,
-0.582692035672022));
#7439=CARTESIAN_POINT('Ctrl Pts',(-0.947476448101718,-0.279889827963178,
-0.604769294586516));
#7440=CARTESIAN_POINT('Ctrl Pts',(-0.919707509403859,-0.251265615809407,
-0.646415841396062));
#7441=CARTESIAN_POINT('Ctrl Pts',(-0.902215926359523,-0.227269801620064,
-0.670378702718353));
#7442=CARTESIAN_POINT('Ctrl Pts',(-0.87482617317514,-0.177024326825049,
-0.705826641853758));
#7443=CARTESIAN_POINT('Ctrl Pts',(-0.861652925570091,-0.144299303100741,
-0.721590372101268));
#7444=CARTESIAN_POINT('Ctrl Pts',(-0.848766861100456,-0.0928409665394229,
-0.736604687327351));
#7445=CARTESIAN_POINT('Ctrl Pts',(-0.84559647055299,-0.0762225747374255,
-0.740223768851063));
#7446=CARTESIAN_POINT('Ctrl Pts',(-0.843383895613249,-0.0595300000000001,
-0.742736168477219));
#7447=CARTESIAN_POINT('',(-0.536443649899847,-0.05953,-0.987512846410683));
#7448=CARTESIAN_POINT('Origin',(0.,-0.05953,0.));
#7449=CARTESIAN_POINT('',(0.0548532617164172,-0.05953,-1.12247250791415));
#7450=CARTESIAN_POINT('Ctrl Pts',(-0.536443649899848,-0.0595300000000001,
-0.987512846410683));
#7451=CARTESIAN_POINT('Ctrl Pts',(-0.533501897135712,-0.0762225747374254,
-0.989110885965947));
#7452=CARTESIAN_POINT('Ctrl Pts',(-0.529268075276156,-0.0928409665394227,
-0.991396466802469));
#7453=CARTESIAN_POINT('Ctrl Pts',(-0.511762781179147,-0.144299303100741,
-1.00061845128527));
#7454=CARTESIAN_POINT('Ctrl Pts',(-0.493462957200432,-0.177024326825049,
-1.0099536580922));
#7455=CARTESIAN_POINT('Ctrl Pts',(-0.45280897844858,-0.227269801620063,
-1.02876878445619));
#7456=CARTESIAN_POINT('Ctrl Pts',(-0.425554672694337,-0.251265615809407,
-1.04048957871266));
#7457=CARTESIAN_POINT('Ctrl Pts',(-0.3787731215897,-0.279889827963178,-1.05829506364875));
#7458=CARTESIAN_POINT('Ctrl Pts',(-0.354166711873529,-0.290879136862659,
-1.06688848765783));
#7459=CARTESIAN_POINT('Ctrl Pts',(-0.302426893214944,-0.305251990234488,
-1.08269251410343));
#7460=CARTESIAN_POINT('Ctrl Pts',(-0.275287440920027,-0.308638795020976,
-1.0898803575765));
#7461=CARTESIAN_POINT('Ctrl Pts',(-0.224855950742601,-0.308638795020976,
-1.10139101611326));
#7462=CARTESIAN_POINT('Ctrl Pts',(-0.19728546073067,-0.305251990234488,
-1.10669035995599));
#7463=CARTESIAN_POINT('Ctrl Pts',(-0.143812384801039,-0.290879136862659,
-1.11490049012186));
#7464=CARTESIAN_POINT('Ctrl Pts',(-0.117914228755037,-0.279889827963178,
-1.1178344036749));
#7465=CARTESIAN_POINT('Ctrl Pts',(-0.0680399972366989,-0.251265615809407,
-1.12208997038458));
#7466=CARTESIAN_POINT('Ctrl Pts',(-0.0383992541984084,-0.227269801620063,
-1.12335509974011));
#7467=CARTESIAN_POINT('Ctrl Pts',(0.00639229239215326,-0.177024326825049,
-1.12404235695137));
#7468=CARTESIAN_POINT('Ctrl Pts',(0.0269302585198977,-0.144299303100741,
-1.12357162229597));
#7469=CARTESIAN_POINT('Ctrl Pts',(0.04670325263426,-0.0928409665394228,
-1.12285816383385));
#7470=CARTESIAN_POINT('Ctrl Pts',(0.0515094706813703,-0.0762225747374255,
-1.12263591311425));
#7471=CARTESIAN_POINT('Ctrl Pts',(0.0548532617164176,-0.0595300000000001,
-1.12247250791414));
#7472=CARTESIAN_POINT('',(0.437601487681057,-0.05953,-1.03511272300331));
#7473=CARTESIAN_POINT('Origin',(0.,-0.05953,0.));
#7474=CARTESIAN_POINT('',(0.911784794170997,-0.05953,-0.656964154625313));
#7475=CARTESIAN_POINT('Ctrl Pts',(0.437601487681056,-0.0595300000000001,
-1.03511272300331));
#7476=CARTESIAN_POINT('Ctrl Pts',(0.440685038163619,-0.0762225747374255,
-1.03380912944435));
#7477=CARTESIAN_POINT('Ctrl Pts',(0.445111721969657,-0.0928409665394228,
-1.03192403056628));
#7478=CARTESIAN_POINT('Ctrl Pts',(0.463236132117164,-0.144299303100741,
-1.0239876538093));
#7479=CARTESIAN_POINT('Ctrl Pts',(0.481944444320713,-0.177024326825049,
-1.01550068154148));
#7480=CARTESIAN_POINT('Ctrl Pts',(0.522002043615455,-0.227269801620064,
-0.995447160474328));
#7481=CARTESIAN_POINT('Ctrl Pts',(0.548158511259203,-0.251265615809407,
-0.981446681891443));
#7482=CARTESIAN_POINT('Ctrl Pts',(0.591247219971725,-0.279889827963178,
-0.955972930713954));
#7483=CARTESIAN_POINT('Ctrl Pts',(0.613307674922609,-0.290879136862659,
-0.942092777160053));
#7484=CARTESIAN_POINT('Ctrl Pts',(0.657923009631182,-0.305251990234487,
-0.91149460735272));
#7485=CARTESIAN_POINT('Ctrl Pts',(0.680463863683393,-0.308638795020976,
-0.894757676234429));
#7486=CARTESIAN_POINT('Ctrl Pts',(0.720906778729542,-0.308638795020976,
-0.862505527716294));
#7487=CARTESIAN_POINT('Ctrl Pts',(0.742239891936899,-0.305251990234488,
-0.844254137480381));
#7488=CARTESIAN_POINT('Ctrl Pts',(0.781998747691872,-0.290879136862659,
-0.80756613568454));
#7489=CARTESIAN_POINT('Ctrl Pts',(0.800439809856112,-0.279889827963178,
-0.789147407129765));
#7490=CARTESIAN_POINT('Ctrl Pts',(0.834863020612702,-0.251265615809407,
-0.752807465209441));
#7491=CARTESIAN_POINT('Ctrl Pts',(0.854332839576145,-0.227269801620064,
-0.73042219438957));
#7492=CARTESIAN_POINT('Ctrl Pts',(0.882797231409153,-0.177024326825049,
-0.695831250979106));
#7493=CARTESIAN_POINT('Ctrl Pts',(0.895234408667242,-0.144299303100741,
-0.679480524217551));
#7494=CARTESIAN_POINT('Ctrl Pts',(0.907004864562642,-0.0928409665394228,
-0.663576540841106));
#7495=CARTESIAN_POINT('Ctrl Pts',(0.909827729890942,-0.0762225747374256,
-0.659680317203144));
#7496=CARTESIAN_POINT('Ctrl Pts',(0.911784794170998,-0.0595300000000001,
-0.656964154625312));
#7497=CARTESIAN_POINT('',(1.08212377959455,-0.05953,-0.303251606722892));
#7498=CARTESIAN_POINT('Origin',(0.,-0.05953,0.));
#7499=CARTESIAN_POINT('',(1.08212377959455,-0.05953,0.303251606722892));
#7500=CARTESIAN_POINT('Ctrl Pts',(1.08212377959455,-0.0595300000000001,
-0.303251606722892));
#7501=CARTESIAN_POINT('Ctrl Pts',(1.0830271513892,-0.0762225747374255,-0.300028012588062));
#7502=CARTESIAN_POINT('Ctrl Pts',(1.08431331394788,-0.0928409665394228,
-0.2953917518996));
#7503=CARTESIAN_POINT('Ctrl Pts',(1.08940878963422,-0.144299303100741,-0.276273267473431));
#7504=CARTESIAN_POINT('Ctrl Pts',(1.09443784939331,-0.177024326825049,-0.256354979351213));
#7505=CARTESIAN_POINT('Ctrl Pts',(1.10373487993589,-0.227269801620064,-0.212533521233765));
#7506=CARTESIAN_POINT('Ctrl Pts',(1.10909715583869,-0.251265615809407,-0.183354415742157));
#7507=CARTESIAN_POINT('Ctrl Pts',(1.1160463456491,-0.279889827963178,-0.133783682657561));
#7508=CARTESIAN_POINT('Ctrl Pts',(1.11894887330541,-0.290879136862659,-0.107881990270302));
#7509=CARTESIAN_POINT('Ctrl Pts',(1.12284346704144,-0.305251990234488,-0.0539226701638766));
#7510=CARTESIAN_POINT('Ctrl Pts',(1.123812,-0.308638795020976,-0.025864214957475));
#7511=CARTESIAN_POINT('Ctrl Pts',(1.123812,-0.308638795020976,0.025864214957475));
#7512=CARTESIAN_POINT('Ctrl Pts',(1.12284346704144,-0.305251990234488,0.0539226701638766));
#7513=CARTESIAN_POINT('Ctrl Pts',(1.11894887330541,-0.290879136862659,0.107881990270302));
#7514=CARTESIAN_POINT('Ctrl Pts',(1.1160463456491,-0.279889827963178,0.133783682657561));
#7515=CARTESIAN_POINT('Ctrl Pts',(1.10909715583869,-0.251265615809407,0.183354415742157));
#7516=CARTESIAN_POINT('Ctrl Pts',(1.10373487993589,-0.227269801620064,0.212533521233765));
#7517=CARTESIAN_POINT('Ctrl Pts',(1.09443784939331,-0.177024326825049,0.256354979351213));
#7518=CARTESIAN_POINT('Ctrl Pts',(1.08940878963422,-0.144299303100741,0.276273267473431));
#7519=CARTESIAN_POINT('Ctrl Pts',(1.08431331394788,-0.0928409665394228,
0.2953917518996));
#7520=CARTESIAN_POINT('Ctrl Pts',(1.0830271513892,-0.0762225747374255,0.300028012588062));
#7521=CARTESIAN_POINT('Ctrl Pts',(1.08212377959455,-0.0595300000000001,
0.303251606722892));
#7522=CARTESIAN_POINT('Origin',(0.,-0.05953,0.));
#7523=CARTESIAN_POINT('Origin',(0.,-0.05953,0.));
#7524=CARTESIAN_POINT('',(0.0589974094846122,-0.05953,1.07456964270265));
#7525=CARTESIAN_POINT('Origin',(0.,-0.05953,0.));
#7526=CARTESIAN_POINT('Origin',(-0.244773027351946,-0.05953,1.07242070340001));
#7527=CARTESIAN_POINT('Origin',(-0.244773027351946,0.,1.07242070340001));
#7528=CARTESIAN_POINT('',(-0.519393123750572,-0.05953,0.942555777842682));
#7529=CARTESIAN_POINT('Ctrl Pts',(-0.519393123750572,-0.05953,0.942555777842682));
#7530=CARTESIAN_POINT('Ctrl Pts',(-0.513714466572041,-0.0925528133349865,
0.945684988399766));
#7531=CARTESIAN_POINT('Ctrl Pts',(-0.503136848051455,-0.124911173756694,
0.951483858396181));
#7532=CARTESIAN_POINT('Ctrl Pts',(-0.47593627990192,-0.177924977804098,
0.965323333309091));
#7533=CARTESIAN_POINT('Ctrl Pts',(-0.460931856495794,-0.199697230012983,
0.972669835243841));
#7534=CARTESIAN_POINT('Ctrl Pts',(-0.426157505475872,-0.237895043532788,
0.988400002689705));
#7535=CARTESIAN_POINT('Ctrl Pts',(-0.406380688682952,-0.254319232363049,
0.996771768218699));
#7536=CARTESIAN_POINT('Ctrl Pts',(-0.364750145543744,-0.28018331644634,
1.01272583306292));
#7537=CARTESIAN_POINT('Ctrl Pts',(-0.340838910881557,-0.29104845371857,
1.02112815447116));
#7538=CARTESIAN_POINT('Ctrl Pts',(-0.290495481564827,-0.30527573347708,
1.036574285215));
#7539=CARTESIAN_POINT('Ctrl Pts',(-0.264056468041074,-0.308638795020976,
1.04359501395068));
#7540=CARTESIAN_POINT('Ctrl Pts',(-0.214892249704082,-0.308638795020976,
1.05481642595959));
#7541=CARTESIAN_POINT('Ctrl Pts',(-0.188025341585962,-0.30527573347708,
1.05996242598502));
#7542=CARTESIAN_POINT('Ctrl Pts',(-0.135965654106109,-0.29104845371857,
1.06788913840721));
#7543=CARTESIAN_POINT('Ctrl Pts',(-0.110776745452494,-0.28018331644634,
1.07069360430242));
#7544=CARTESIAN_POINT('Ctrl Pts',(-0.0663467128214646,-0.254319232363049,
1.07438230428002));
#7545=CARTESIAN_POINT('Ctrl Pts',(-0.0448960436540983,-0.237895043532788,
1.07542044338697));
#7546=CARTESIAN_POINT('Ctrl Pts',(-0.00674037211528124,-0.199697230012983,
1.07633607767727));
#7547=CARTESIAN_POINT('Ctrl Pts',(0.00996567398334777,-0.177924977804098,
1.07622728347683));
#7548=CARTESIAN_POINT('Ctrl Pts',(0.0404772621979741,-0.124911173756694,
1.07556023164702));
#7549=CARTESIAN_POINT('Ctrl Pts',(0.0525234025782719,-0.0925528133349865,
1.07492508698591));
#7550=CARTESIAN_POINT('Ctrl Pts',(0.0589974094846124,-0.05953,1.07456964270265));
#7551=CARTESIAN_POINT('Origin',(-0.244773027351946,-0.05953,1.07242070340001));
#7552=CARTESIAN_POINT('Origin',(0.,-0.05953,0.));
#7553=CARTESIAN_POINT('',(-0.803348093619616,-0.05953,0.716109245731214));
#7554=CARTESIAN_POINT('Origin',(0.,-0.05953,0.));
#7555=CARTESIAN_POINT('Origin',(-0.991065754692661,-0.05953,0.477272113029314));
#7556=CARTESIAN_POINT('Origin',(-0.991065754692661,0.,0.477272113029314));
#7557=CARTESIAN_POINT('',(-1.06075609691358,-0.05953,0.181596019242328));
#7558=CARTESIAN_POINT('Ctrl Pts',(-1.06075609691358,-0.05953,0.181596019242328));
#7559=CARTESIAN_POINT('Ctrl Pts',(-1.05966202740332,-0.0925528133349865,
0.187986803072856));
#7560=CARTESIAN_POINT('Ctrl Pts',(-1.05760072925372,-0.124911173756694,
0.199872254546857));
#7561=CARTESIAN_POINT('Ctrl Pts',(-1.05146158959546,-0.177924977804098,
0.22976728653846));
#7562=CARTESIAN_POINT('Ctrl Pts',(-1.04785021111757,-0.199697230012983,
0.246078686169301));
#7563=CARTESIAN_POINT('Ctrl Pts',(-1.03846709802406,-0.237895043532788,
0.283073967563097));
#7564=CARTESIAN_POINT('Ctrl Pts',(-1.03268176429485,-0.254319232363049,
0.303755815985685));
#7565=CARTESIAN_POINT('Ctrl Pts',(-1.01919893537026,-0.28018331644634,0.346251081972725));
#7566=CARTESIAN_POINT('Ctrl Pts',(-1.01085972381132,-0.29104845371857,0.370184399726282));
#7567=CARTESIAN_POINT('Ctrl Pts',(-0.99154738033959,-0.30527573347708,0.419174982698463));
#7568=CARTESIAN_POINT('Ctrl Pts',(-0.980551951791748,-0.308638795020976,
0.444223188605045));
#7569=CARTESIAN_POINT('Ctrl Pts',(-0.958671816228589,-0.308638795020976,
0.489657758261848));
#7570=CARTESIAN_POINT('Ctrl Pts',(-0.945943877838127,-0.30527573347708,
0.51387163140139));
#7571=CARTESIAN_POINT('Ctrl Pts',(-0.91968254693063,-0.29104845371857,0.559515758398093));
#7572=CARTESIAN_POINT('Ctrl Pts',(-0.906170138993533,-0.28018331644634,
0.580957796077825));
#7573=CARTESIAN_POINT('Ctrl Pts',(-0.8813524085237,-0.254319232363049,0.617994461173994));
#7574=CARTESIAN_POINT('Ctrl Pts',(-0.868789784891799,-0.237895043532788,
0.635412538795143));
#7575=CARTESIAN_POINT('Ctrl Pts',(-0.845715984518854,-0.199697230012983,
0.66581473268113));
#7576=CARTESIAN_POINT('Ctrl Pts',(-0.835214876415962,-0.177924977804098,
0.678808213394124));
#7577=CARTESIAN_POINT('Ctrl Pts',(-0.815669690204649,-0.124911173756694,
0.702247233627224));
#7578=CARTESIAN_POINT('Ctrl Pts',(-0.807662468433796,-0.0925528133349865,
0.711269279199861));
#7579=CARTESIAN_POINT('Ctrl Pts',(-0.803348093619616,-0.05953,0.716109245731214));
#7580=CARTESIAN_POINT('Origin',(-0.991065754692661,-0.05953,0.477272113029314));
#7581=CARTESIAN_POINT('Origin',(0.,-0.05953,0.));
#7582=CARTESIAN_POINT('',(-1.076188,-0.05953,1.31795018948079E-16));
#7583=CARTESIAN_POINT('Origin',(0.,-0.05953,0.));
#7584=CARTESIAN_POINT('',(-1.06075609691358,-0.05953,-0.181596019242328));
#7585=CARTESIAN_POINT('Origin',(0.,-0.05953,0.));
#7586=CARTESIAN_POINT('Origin',(-0.991065754692661,-0.05953,-0.477272113029314));
#7587=CARTESIAN_POINT('Origin',(-0.991065754692661,0.,-0.477272113029314));
#7588=CARTESIAN_POINT('',(-0.803348093619616,-0.05953,-0.716109245731215));
#7589=CARTESIAN_POINT('Ctrl Pts',(-0.803348093619616,-0.05953,-0.716109245731215));
#7590=CARTESIAN_POINT('Ctrl Pts',(-0.807662468433795,-0.0925528133349865,
-0.711269279199862));
#7591=CARTESIAN_POINT('Ctrl Pts',(-0.815669690204649,-0.124911173756694,
-0.702247233627224));
#7592=CARTESIAN_POINT('Ctrl Pts',(-0.835214876415962,-0.177924977804098,
-0.678808213394124));
#7593=CARTESIAN_POINT('Ctrl Pts',(-0.845715984518854,-0.199697230012983,
-0.66581473268113));
#7594=CARTESIAN_POINT('Ctrl Pts',(-0.868789784891799,-0.237895043532788,
-0.635412538795143));
#7595=CARTESIAN_POINT('Ctrl Pts',(-0.8813524085237,-0.254319232363049,-0.617994461173994));
#7596=CARTESIAN_POINT('Ctrl Pts',(-0.906170138993533,-0.28018331644634,
-0.580957796077826));
#7597=CARTESIAN_POINT('Ctrl Pts',(-0.91968254693063,-0.29104845371857,-0.559515758398093));
#7598=CARTESIAN_POINT('Ctrl Pts',(-0.945943877838127,-0.30527573347708,
-0.51387163140139));
#7599=CARTESIAN_POINT('Ctrl Pts',(-0.958671816228589,-0.308638795020976,
-0.489657758261848));
#7600=CARTESIAN_POINT('Ctrl Pts',(-0.980551951791748,-0.308638795020976,
-0.444223188605045));
#7601=CARTESIAN_POINT('Ctrl Pts',(-0.99154738033959,-0.30527573347708,-0.419174982698463));
#7602=CARTESIAN_POINT('Ctrl Pts',(-1.01085972381132,-0.29104845371857,-0.370184399726282));
#7603=CARTESIAN_POINT('Ctrl Pts',(-1.01919893537026,-0.28018331644634,-0.346251081972725));
#7604=CARTESIAN_POINT('Ctrl Pts',(-1.03268176429485,-0.254319232363049,
-0.303755815985685));
#7605=CARTESIAN_POINT('Ctrl Pts',(-1.03846709802406,-0.237895043532788,
-0.283073967563097));
#7606=CARTESIAN_POINT('Ctrl Pts',(-1.04785021111757,-0.199697230012983,
-0.246078686169302));
#7607=CARTESIAN_POINT('Ctrl Pts',(-1.05146158959546,-0.177924977804098,
-0.229767286538461));
#7608=CARTESIAN_POINT('Ctrl Pts',(-1.05760072925372,-0.124911173756694,
-0.199872254546858));
#7609=CARTESIAN_POINT('Ctrl Pts',(-1.05966202740332,-0.0925528133349864,
-0.187986803072857));
#7610=CARTESIAN_POINT('Ctrl Pts',(-1.06075609691358,-0.05953,-0.181596019242328));
#7611=CARTESIAN_POINT('Origin',(-0.991065754692661,-0.05953,-0.477272113029314));
#7612=CARTESIAN_POINT('Origin',(0.,-0.05953,0.));
#7613=CARTESIAN_POINT('',(-0.519393123750572,-0.05953,-0.942555777842682));
#7614=CARTESIAN_POINT('Origin',(0.,-0.05953,0.));
#7615=CARTESIAN_POINT('Origin',(-0.244773027351946,-0.05953,-1.07242070340001));
#7616=CARTESIAN_POINT('Origin',(-0.244773027351946,0.,-1.07242070340001));
#7617=CARTESIAN_POINT('',(0.0589974094846125,-0.05953,-1.07456964270265));
#7618=CARTESIAN_POINT('Ctrl Pts',(0.0589974094846127,-0.05953,-1.07456964270265));
#7619=CARTESIAN_POINT('Ctrl Pts',(0.0525234025782722,-0.0925528133349865,
-1.07492508698591));
#7620=CARTESIAN_POINT('Ctrl Pts',(0.0404772621979744,-0.124911173756694,
-1.07556023164702));
#7621=CARTESIAN_POINT('Ctrl Pts',(0.0099656739833481,-0.177924977804098,
-1.07622728347683));
#7622=CARTESIAN_POINT('Ctrl Pts',(-0.00674037211528096,-0.199697230012983,
-1.07633607767727));
#7623=CARTESIAN_POINT('Ctrl Pts',(-0.044896043654098,-0.237895043532788,
-1.07542044338697));
#7624=CARTESIAN_POINT('Ctrl Pts',(-0.0663467128214644,-0.254319232363049,
-1.07438230428002));
#7625=CARTESIAN_POINT('Ctrl Pts',(-0.110776745452493,-0.28018331644634,
-1.07069360430242));
#7626=CARTESIAN_POINT('Ctrl Pts',(-0.135965654106109,-0.29104845371857,
-1.06788913840721));
#7627=CARTESIAN_POINT('Ctrl Pts',(-0.188025341585962,-0.30527573347708,
-1.05996242598502));
#7628=CARTESIAN_POINT('Ctrl Pts',(-0.214892249704082,-0.308638795020976,
-1.05481642595959));
#7629=CARTESIAN_POINT('Ctrl Pts',(-0.264056468041074,-0.308638795020976,
-1.04359501395068));
#7630=CARTESIAN_POINT('Ctrl Pts',(-0.290495481564827,-0.30527573347708,
-1.036574285215));
#7631=CARTESIAN_POINT('Ctrl Pts',(-0.340838910881557,-0.291048453718569,
-1.02112815447116));
#7632=CARTESIAN_POINT('Ctrl Pts',(-0.364750145543744,-0.28018331644634,
-1.01272583306292));
#7633=CARTESIAN_POINT('Ctrl Pts',(-0.406380688682952,-0.254319232363049,
-0.996771768218699));
#7634=CARTESIAN_POINT('Ctrl Pts',(-0.426157505475872,-0.237895043532788,
-0.988400002689705));
#7635=CARTESIAN_POINT('Ctrl Pts',(-0.460931856495794,-0.199697230012983,
-0.972669835243841));
#7636=CARTESIAN_POINT('Ctrl Pts',(-0.475936279901919,-0.177924977804098,
-0.965323333309091));
#7637=CARTESIAN_POINT('Ctrl Pts',(-0.503136848051454,-0.124911173756694,
-0.951483858396181));
#7638=CARTESIAN_POINT('Ctrl Pts',(-0.513714466572041,-0.0925528133349865,
-0.945684988399766));
#7639=CARTESIAN_POINT('Ctrl Pts',(-0.519393123750572,-0.05953,-0.942555777842682));
#7640=CARTESIAN_POINT('Origin',(-0.244773027351946,-0.05953,-1.07242070340001));
#7641=CARTESIAN_POINT('Origin',(0.,-0.05953,0.));
#7642=CARTESIAN_POINT('',(0.413083465285518,-0.05953,-0.993751811093549));
#7643=CARTESIAN_POINT('Origin',(0.,-0.05953,0.));
#7644=CARTESIAN_POINT('Origin',(0.685838782044607,-0.05953,-0.860014630714833));
#7645=CARTESIAN_POINT('Origin',(0.685838782044607,0.,-0.860014630714833));
#7646=CARTESIAN_POINT('',(0.876916659919095,-0.05953,-0.623857181492959));
#7647=CARTESIAN_POINT('Ctrl Pts',(0.876916659919095,-0.05953,-0.623857181492958));
#7648=CARTESIAN_POINT('Ctrl Pts',(0.873158080166742,-0.0925528133349865,
-0.62914037979579));
#7649=CARTESIAN_POINT('Ctrl Pts',(0.866144010579847,-0.124911173756694,
-0.638954437806245));
#7650=CARTESIAN_POINT('Ctrl Pts',(0.847641868610495,-0.177924977804098,
-0.663225258065736));
#7651=CARTESIAN_POINT('Ctrl Pts',(0.837310877969633,-0.199697230012983,
-0.676354402927683));
#7652=CARTESIAN_POINT('Ctrl Pts',(0.81280533416753,-0.237895043532788,-0.705614819529209));
#7653=CARTESIAN_POINT('Ctrl Pts',(0.798619410861634,-0.254319232363049,
-0.721738358858166));
#7654=CARTESIAN_POINT('Ctrl Pts',(0.768033796848072,-0.28018331644634,-0.754175290318038));
#7655=CARTESIAN_POINT('Ctrl Pts',(0.750136149454208,-0.29104845371857,-0.772120216227122));
#7656=CARTESIAN_POINT('Ctrl Pts',(0.711480111898423,-0.30527573347708,-0.807879894508811));
#7657=CARTESIAN_POINT('Ctrl Pts',(0.690705563850638,-0.308638795020976,
-0.825676810575913));
#7658=CARTESIAN_POINT('Ctrl Pts',(0.651278921914856,-0.308638795020976,
-0.857118508332695));
#7659=CARTESIAN_POINT('Ctrl Pts',(0.629305439856167,-0.30527573347708,-0.873412008702649));
#7660=CARTESIAN_POINT('Ctrl Pts',(0.585840553788742,-0.29104845371857,-0.903141581680914));
#7661=CARTESIAN_POINT('Ctrl Pts',(0.564362943424239,-0.28018331644634,-0.916597376014514));
#7662=CARTESIAN_POINT('Ctrl Pts',(0.525933334162556,-0.254319232363049,
-0.939198248544427));
#7663=CARTESIAN_POINT('Ctrl Pts',(0.507057380724533,-0.237895043532788,
-0.949440676105255));
#7664=CARTESIAN_POINT('Ctrl Pts',(0.473077587363686,-0.199697230012983,
-0.966820759530997));
#7665=CARTESIAN_POINT('Ctrl Pts',(0.457978755888596,-0.177924977804098,
-0.973971221090534));
#7666=CARTESIAN_POINT('Ctrl Pts',(0.430199341854858,-0.124911173756694,
-0.986608710139579));
#7667=CARTESIAN_POINT('Ctrl Pts',(0.419070565453384,-0.0925528133349865,
-0.991263089003441));
#7668=CARTESIAN_POINT('Ctrl Pts',(0.413083465285518,-0.05953,-0.993751811093549));
#7669=CARTESIAN_POINT('Origin',(0.685838782044607,-0.05953,-0.860014630714833));
#7670=CARTESIAN_POINT('Origin',(0.,-0.208355,0.));
#7671=CARTESIAN_POINT('',(-1.076188,-0.35718,1.31795018948079E-16));
#7672=CARTESIAN_POINT('Origin',(0.,-0.35718,0.));
#7673=CARTESIAN_POINT('',(-1.076188,-0.208355,1.31795018948079E-16));
#7674=CARTESIAN_POINT('',(1.03449977959455,-0.05953,0.296632461748266));
#7675=CARTESIAN_POINT('Origin',(0.,-0.05953,0.));
#7676=CARTESIAN_POINT('',(1.03449977959455,-0.05953,-0.296632461748266));
#7677=CARTESIAN_POINT('Ctrl Pts',(1.03449977959455,-0.05953,0.296632461748267));
#7678=CARTESIAN_POINT('Ctrl Pts',(1.03628691421076,-0.0925528133349865,
0.290399865505497));
#7679=CARTESIAN_POINT('Ctrl Pts',(1.03958665287714,-0.124911173756694,0.278797079997872));
#7680=CARTESIAN_POINT('Ctrl Pts',(1.0470264474309,-0.177924977804098,0.249198913998601));
#7681=CARTESIAN_POINT('Ctrl Pts',(1.05084995891418,-0.199697230012983,0.232935932341942));
#7682=CARTESIAN_POINT('Ctrl Pts',(1.05844771715377,-0.237895043532788,0.195533155353269));
#7683=CARTESIAN_POINT('Ctrl Pts',(1.06220882929878,-0.254319232363049,0.17438929156337));
#7684=CARTESIAN_POINT('Ctrl Pts',(1.06849922508772,-0.28018331644634,0.130252399648131));
#7685=CARTESIAN_POINT('Ctrl Pts',(1.07137013248666,-0.29104845371857,0.105070977154072));
#7686=CARTESIAN_POINT('Ctrl Pts',(1.07522652957392,-0.30527573347708,0.0525526752791107));
#7687=CARTESIAN_POINT('Ctrl Pts',(1.076188,-0.308638795020976,0.025214283908933));
#7688=CARTESIAN_POINT('Ctrl Pts',(1.076188,-0.308638795020976,-0.025214283908933));
#7689=CARTESIAN_POINT('Ctrl Pts',(1.07522652957392,-0.30527573347708,-0.0525526752791107));
#7690=CARTESIAN_POINT('Ctrl Pts',(1.07137013248666,-0.29104845371857,-0.105070977154072));
#7691=CARTESIAN_POINT('Ctrl Pts',(1.06849922508772,-0.28018331644634,-0.130252399648131));
#7692=CARTESIAN_POINT('Ctrl Pts',(1.06220882929878,-0.254319232363049,-0.17438929156337));
#7693=CARTESIAN_POINT('Ctrl Pts',(1.05844771715377,-0.237895043532788,-0.195533155353269));
#7694=CARTESIAN_POINT('Ctrl Pts',(1.05084995891418,-0.199697230012983,-0.232935932341942));
#7695=CARTESIAN_POINT('Ctrl Pts',(1.0470264474309,-0.177924977804098,-0.249198913998601));
#7696=CARTESIAN_POINT('Ctrl Pts',(1.03958665287714,-0.124911173756694,-0.278797079997872));
#7697=CARTESIAN_POINT('Ctrl Pts',(1.03628691421076,-0.0925528133349865,
-0.290399865505497));
#7698=CARTESIAN_POINT('Ctrl Pts',(1.03449977959455,-0.05953,-0.296632461748267));
#7699=CARTESIAN_POINT('Origin',(0.,-0.05953,0.));
#7700=CARTESIAN_POINT('Origin',(0.,-0.05953,0.));
#7701=CARTESIAN_POINT('Origin',(1.1,-0.05953,0.));
#7702=CARTESIAN_POINT('Origin',(1.1,0.,0.));
#7703=CARTESIAN_POINT('Origin',(1.1,-0.05953,0.));
#7704=CARTESIAN_POINT('Origin',(0.,-0.35718,0.));
#7705=CARTESIAN_POINT('Origin',(0.,-0.05953,0.));
#7786=UNCERTAINTY_MEASURE_WITH_UNIT(LENGTH_MEASURE(0.001),#7817,
'DISTANCE_ACCURACY_VALUE',
'Maximum model space distance between geometric entities at asserted c
onnectivities');
#7789=UNCERTAINTY_MEASURE_WITH_UNIT(LENGTH_MEASURE(0.001),#7817,
'DISTANCE_ACCURACY_VALUE',
'Maximum model space distance between geometric entities at asserted c
onnectivities');
#7813=(
GEOMETRIC_REPRESENTATION_CONTEXT(3)
GLOBAL_UNCERTAINTY_ASSIGNED_CONTEXT((#7786))
GLOBAL_UNIT_ASSIGNED_CONTEXT((#7817,#7819,#7820))
REPRESENTATION_CONTEXT('','3D')
);
#7816=(
GEOMETRIC_REPRESENTATION_CONTEXT(3)
GLOBAL_UNCERTAINTY_ASSIGNED_CONTEXT((#7789))
GLOBAL_UNIT_ASSIGNED_CONTEXT((#7817,#7819,#7820))
REPRESENTATION_CONTEXT('','3D')
);
#7817=(
LENGTH_UNIT()
NAMED_UNIT(*)
SI_UNIT(.CENTI.,.METRE.)
);
#7819=(
NAMED_UNIT(*)
PLANE_ANGLE_UNIT()
SI_UNIT($,.RADIAN.)
);
#7820=(
NAMED_UNIT(*)
SI_UNIT($,.STERADIAN.)
SOLID_ANGLE_UNIT()
);
#7844=SHAPE_DEFINITION_REPRESENTATION(#7885,#7924);
#7885=PRODUCT_DEFINITION_SHAPE('',$,#7951);
#7924=SHAPE_REPRESENTATION('',(#4400),#7813);
#7927=PRODUCT_DEFINITION_CONTEXT('part definition',#8007,'design');
#7951=PRODUCT_DEFINITION('Cage (1)','Cage (1)',#7977,#7927);
#7977=PRODUCT_DEFINITION_FORMATION('',$,#8032);
#8007=APPLICATION_CONTEXT(
'Core Data for Automotive Mechanical Design Process');
#8008=PRODUCT_CONTEXT('part definition',#8007,'mechanical');
#8032=PRODUCT('Cage (1)','Cage (1)','Cage (1)',(#8008));
#8091=COLOUR_RGB('Grey',0.48,0.52,0.57);
#8092=FILL_AREA_STYLE_COLOUR('',#8091);
#8093=FILL_AREA_STYLE('',(#8092));
#8094=SURFACE_STYLE_FILL_AREA(#8093);
#8095=SURFACE_SIDE_STYLE('',(#8094));
#8096=SURFACE_STYLE_USAGE(.BOTH.,#8095);
#8097=PRESENTATION_STYLE_ASSIGNMENT((#8096));
ENDSEC;
END-ISO-10303-21;
